ISO-10303-21;
HEADER;
/* Generated by software containing ST-Developer
 * from STEP Tools, Inc. (www.steptools.com) 
 */

FILE_DESCRIPTION(
/* description */ ('Hand wheel with handle and shaft collar'),
/* implementation_level */ '2;1');

FILE_NAME(
/* name */ 'Bonded pad (1).step',
/* time_stamp */ '2026-10-28T03:23:19-07:00',
/* author */ (''),
/* organization */ (''),
/* preprocessor_version */ 'ST-DEVELOPER v20.2',
/* originating_system */ 'Autodesk Translation Framework v15.17.0.0',
/* authorisation */ '');

FILE_SCHEMA (('AUTOMOTIVE_DESIGN { 1 0 10303 214 3 1 1 }'));
ENDSEC;

DATA;
#10=MECHANICAL_DESIGN_GEOMETRIC_PRESENTATION_REPRESENTATION('',(#397),#10510);
#333=SHAPE_REPRESENTATION_RELATIONSHIP('SRR','None',#10649,#365);
#365=ADVANCED_BREP_SHAPE_REPRESENTATION('',(#444),#10476);
#397=STYLED_ITEM('',(#10922),#444);
#444=MANIFOLD_SOLID_BREP('Body1',#5296);
#610=PLANE('',#5726);
#611=PLANE('',#5727);
#612=PLANE('',#5728);
#613=PLANE('',#5729);
#614=PLANE('',#5730);
#615=PLANE('',#5731);
#779=FACE_OUTER_BOUND('',#1106,.T.);
#780=FACE_OUTER_BOUND('',#1107,.T.);
#781=FACE_OUTER_BOUND('',#1108,.T.);
#782=FACE_OUTER_BOUND('',#1109,.T.);
#783=FACE_OUTER_BOUND('',#1110,.T.);
#784=FACE_OUTER_BOUND('',#1111,.T.);
#1106=EDGE_LOOP('',(#3629,#3630,#3631,#3632));
#1107=EDGE_LOOP('',(#3633,#3634,#3635,#3636));
#1108=EDGE_LOOP('',(#3637,#3638,#3639,#3640));
#1109=EDGE_LOOP('',(#3641,#3642,#3643,#3644));
#1110=EDGE_LOOP('',(#3645,#3646,#3647,#3648));
#1111=EDGE_LOOP('',(#3649,#3650,#3651,#3652));
#1541=LINE('',#8257,#1851);
#1542=LINE('',#8259,#1852);
#1543=LINE('',#8261,#1853);
#1544=LINE('',#8262,#1854);
#1545=LINE('',#8265,#1855);
#1546=LINE('',#8267,#1856);
#1547=LINE('',#8268,#1857);
#1548=LINE('',#8271,#1858);
#1549=LINE('',#8273,#1859);
#1550=LINE('',#8274,#1860);
#1551=LINE('',#8276,#1861);
#1552=LINE('',#8277,#1862);
#1851=VECTOR('',#6507,1.);
#1852=VECTOR('',#6508,1.);
#1853=VECTOR('',#6509,1.);
#1854=VECTOR('',#6510,1.);
#1855=VECTOR('',#6513,1.);
#1856=VECTOR('',#6514,1.);
#1857=VECTOR('',#6515,1.);
#1858=VECTOR('',#6518,1.);
#1859=VECTOR('',#6519,1.);
#1860=VECTOR('',#6520,1.);
#1861=VECTOR('',#6523,1.);
#1862=VECTOR('',#6524,1.);
#2468=VERTEX_POINT('',#8255);
#2469=VERTEX_POINT('',#8256);
#2470=VERTEX_POINT('',#8258);
#2471=VERTEX_POINT('',#8260);
#2472=VERTEX_POINT('',#8264);
#2473=VERTEX_POINT('',#8266);
#2474=VERTEX_POINT('',#8270);
#2475=VERTEX_POINT('',#8272);
#2932=EDGE_CURVE('',#2468,#2469,#1541,.T.);
#2933=EDGE_CURVE('',#2469,#2470,#1542,.T.);
#2934=EDGE_CURVE('',#2471,#2470,#1543,.T.);
#2935=EDGE_CURVE('',#2468,#2471,#1544,.T.);
#2936=EDGE_CURVE('',#2472,#2468,#1545,.T.);
#2937=EDGE_CURVE('',#2473,#2471,#1546,.T.);
#2938=EDGE_CURVE('',#2472,#2473,#1547,.T.);
#2939=EDGE_CURVE('',#2474,#2472,#1548,.T.);
#2940=EDGE_CURVE('',#2475,#2473,#1549,.T.);
#2941=EDGE_CURVE('',#2474,#2475,#1550,.T.);
#2942=EDGE_CURVE('',#2469,#2474,#1551,.T.);
#2943=EDGE_CURVE('',#2470,#2475,#1552,.T.);
#3629=ORIENTED_EDGE('',*,*,#2932,.T.);
#3630=ORIENTED_EDGE('',*,*,#2933,.T.);
#3631=ORIENTED_EDGE('',*,*,#2934,.F.);
#3632=ORIENTED_EDGE('',*,*,#2935,.F.);
#3633=ORIENTED_EDGE('',*,*,#2936,.T.);
#3634=ORIENTED_EDGE('',*,*,#2935,.T.);
#3635=ORIENTED_EDGE('',*,*,#2937,.F.);
#3636=ORIENTED_EDGE('',*,*,#2938,.F.);
#3637=ORIENTED_EDGE('',*,*,#2939,.T.);
#3638=ORIENTED_EDGE('',*,*,#2938,.T.);
#3639=ORIENTED_EDGE('',*,*,#2940,.F.);
#3640=ORIENTED_EDGE('',*,*,#2941,.F.);
#3641=ORIENTED_EDGE('',*,*,#2942,.T.);
#3642=ORIENTED_EDGE('',*,*,#2941,.T.);
#3643=ORIENTED_EDGE('',*,*,#2943,.F.);
#3644=ORIENTED_EDGE('',*,*,#2933,.F.);
#3645=ORIENTED_EDGE('',*,*,#2943,.T.);
#3646=ORIENTED_EDGE('',*,*,#2940,.T.);
#3647=ORIENTED_EDGE('',*,*,#2937,.T.);
#3648=ORIENTED_EDGE('',*,*,#2934,.T.);
#3649=ORIENTED_EDGE('',*,*,#2942,.F.);
#3650=ORIENTED_EDGE('',*,*,#2932,.F.);
#3651=ORIENTED_EDGE('',*,*,#2936,.F.);
#3652=ORIENTED_EDGE('',*,*,#2939,.F.);
#4991=ADVANCED_FACE('',(#779),#610,.T.);
#4992=ADVANCED_FACE('',(#780),#611,.T.);
#4993=ADVANCED_FACE('',(#781),#612,.T.);
#4994=ADVANCED_FACE('',(#782),#613,.T.);
#4995=ADVANCED_FACE('',(#783),#614,.T.);
#4996=ADVANCED_FACE('',(#784),#615,.F.);
#5296=CLOSED_SHELL('',(#4991,#4992,#4993,#4994,#4995,#4996));
#5725=AXIS2_PLACEMENT_3D('',#8253,#6503,#6504);
#5726=AXIS2_PLACEMENT_3D('',#8254,#6505,#6506);
#5727=AXIS2_PLACEMENT_3D('',#8263,#6511,#6512);
#5728=AXIS2_PLACEMENT_3D('',#8269,#6516,#6517);
#5729=AXIS2_PLACEMENT_3D('',#8275,#6521,#6522);
#5730=AXIS2_PLACEMENT_3D('',#8278,#6525,#6526);
#5731=AXIS2_PLACEMENT_3D('',#8279,#6527,#6528);
#6503=DIRECTION('axis',(0.,0.,1.));
#6504=DIRECTION('refdir',(1.,0.,0.));
#6505=DIRECTION('center_axis',(0.,1.,0.));
#6506=DIRECTION('ref_axis',(-1.,0.,0.));
#6507=DIRECTION('',(-1.,0.,0.));
#6508=DIRECTION('',(0.,0.,1.));
#6509=DIRECTION('',(-1.,0.,0.));
#6510=DIRECTION('',(0.,0.,1.));
#6511=DIRECTION('center_axis',(1.,0.,0.));
#6512=DIRECTION('ref_axis',(0.,1.,0.));
#6513=DIRECTION('',(0.,1.,0.));
#6514=DIRECTION('',(0.,1.,0.));
#6515=DIRECTION('',(0.,0.,1.));
#6516=DIRECTION('center_axis',(0.,-1.,0.));
#6517=DIRECTION('ref_axis',(1.,0.,0.));
#6518=DIRECTION('',(1.,0.,0.));
#6519=DIRECTION('',(1.,0.,0.));
#6520=DIRECTION('',(0.,0.,1.));
#6521=DIRECTION('center_axis',(-1.,0.,0.));
#6522=DIRECTION('ref_axis',(0.,-1.,0.));
#6523=DIRECTION('',(0.,-1.,0.));
#6524=DIRECTION('',(0.,-1.,0.));
#6525=DIRECTION('center_axis',(0.,0.,1.));
#6526=DIRECTION('ref_axis',(1.,0.,0.));
#6527=DIRECTION('center_axis',(0.,0.,1.));
#6528=DIRECTION('ref_axis',(1.,0.,0.));
#8253=CARTESIAN_POINT('',(0.,0.,0.));
#8254=CARTESIAN_POINT('Origin',(9.5,7.,-0.3));
#8255=CARTESIAN_POINT('',(9.5,7.,-0.3));
#8256=CARTESIAN_POINT('',(7.5,7.,-0.3));
#8257=CARTESIAN_POINT('',(9.5,7.,-0.3));
#8258=CARTESIAN_POINT('',(7.5,7.,0.));
#8259=CARTESIAN_POINT('',(7.5,7.,-0.3));
#8260=CARTESIAN_POINT('',(9.5,7.,0.));
#8261=CARTESIAN_POINT('',(9.5,7.,0.));
#8262=CARTESIAN_POINT('',(9.5,7.,-0.3));
#8263=CARTESIAN_POINT('Origin',(9.5,-1.,-0.3));
#8264=CARTESIAN_POINT('',(9.5,-1.,-0.3));
#8265=CARTESIAN_POINT('',(9.5,-1.,-0.3));
#8266=CARTESIAN_POINT('',(9.5,-1.,0.));
#8267=CARTESIAN_POINT('',(9.5,-1.,0.));
#8268=CARTESIAN_POINT('',(9.5,-1.,-0.3));
#8269=CARTESIAN_POINT('Origin',(7.5,-1.,-0.3));
#8270=CARTESIAN_POINT('',(7.5,-1.,-0.3));
#8271=CARTESIAN_POINT('',(7.5,-1.,-0.3));
#8272=CARTESIAN_POINT('',(7.5,-1.,0.));
#8273=CARTESIAN_POINT('',(7.5,-1.,0.));
#8274=CARTESIAN_POINT('',(7.5,-1.,-0.3));
#8275=CARTESIAN_POINT('Origin',(7.5,7.,-0.3));
#8276=CARTESIAN_POINT('',(7.5,7.,-0.3));
#8277=CARTESIAN_POINT('',(7.5,7.,0.));
#8278=CARTESIAN_POINT('Origin',(8.5,3.,0.));
#8279=CARTESIAN_POINT('Origin',(8.5,3.,-0.3));
#10437=UNCERTAINTY_MEASURE_WITH_UNIT(LENGTH_MEASURE(0.001),#10511,
'DISTANCE_ACCURACY_VALUE',
'Maximum model space distance between geometric entities at asserted c
onnectivities');
#10471=UNCERTAINTY_MEASURE_WITH_UNIT(LENGTH_MEASURE(0.001),#10511,
'DISTANCE_ACCURACY_VALUE',
'Maximum model space distance between geometric entities at asserted c
onnectivities');
#10476=(
GEOMETRIC_REPRESENTATION_CONTEXT(3)
GLOBAL_UNCERTAINTY_ASSIGNED_CONTEXT((#10437))
GLOBAL_UNIT_ASSIGNED_CONTEXT((#10511,#10513,#10514))
REPRESENTATION_CONTEXT('','3D')
);
#10510=(
GEOMETRIC_REPRESENTATION_CONTEXT(3)
GLOBAL_UNCERTAINTY_ASSIGNED_CONTEXT((#10471))
GLOBAL_UNIT_ASSIGNED_CONTEXT((#10511,#10513,#10514))
REPRESENTATION_CONTEXT('','3D')
);
#10511=(
LENGTH_UNIT()
NAMED_UNIT(*)
SI_UNIT(.CENTI.,.METRE.)
);
#10513=(
NAMED_UNIT(*)
PLANE_ANGLE_UNIT()
SI_UNIT($,.RADIAN.)
);
#10514=(
NAMED_UNIT(*)
SI_UNIT($,.STERADIAN.)
SOLID_ANGLE_UNIT()
);
#10519=SHAPE_DEFINITION_REPRESENTATION(#10557,#10649);
#10557=PRODUCT_DEFINITION_SHAPE('',$,#10688);
#10649=SHAPE_REPRESENTATION('',(#5725),#10476);
#10683=PRODUCT_DEFINITION_CONTEXT('part definition',#10799,'design');
#10688=PRODUCT_DEFINITION('Bonded pad (1)','Bonded pad (1)',#10726,#10683);
#10726=PRODUCT_DEFINITION_FORMATION('',$,#10805);
#10799=APPLICATION_CONTEXT(
'Core Data for Automotive Mechanical Design Process');
#10800=PRODUCT_CONTEXT('part definition',#10799,'mechanical');
#10805=PRODUCT('Bonded pad (1)','Bonded pad (1)','Bonded pad (1)',(#10800));
#10916=COLOUR_RGB('Off White',0.89,0.88,0.83);
#10917=FILL_AREA_STYLE_COLOUR('',#10916);
#10918=FILL_AREA_STYLE('',(#10917));
#10919=SURFACE_STYLE_FILL_AREA(#10918);
#10920=SURFACE_SIDE_STYLE('',(#10919));
#10921=SURFACE_STYLE_USAGE(.BOTH.,#10920);
#10922=PRESENTATION_STYLE_ASSIGNMENT((#10921));
ENDSEC;
END-ISO-10303-21;
